ISO-10303-21;
HEADER;
/* Generated by software containing ST-Developer
 * from STEP Tools, Inc. (www.steptools.com) 
 */

FILE_DESCRIPTION(
/* description */ (''),
/* implementation_level */ '2;1');

FILE_NAME(
/* name */ 'Nut_02.step',
/* time_stamp */ '2026-10-06T13:15:55-07:00',
/* author */ (''),
/* organization */ (''),
/* preprocessor_version */ 'ST-DEVELOPER v20.2',
/* originating_system */ 'Autodesk Translation Framework v15.15.0.0',
/* authorisation */ '');

FILE_SCHEMA (('AUTOMOTIVE_DESIGN { 1 0 10303 214 3 1 1 }'));
ENDSEC;

DATA;
#10=MECHANICAL_DESIGN_GEOMETRIC_PRESENTATION_REPRESENTATION('',(#110),#27707);
#90=SHAPE_REPRESENTATION_RELATIONSHIP('SRR','None',#27747,#100);
#100=ADVANCED_BREP_SHAPE_REPRESENTATION('',(#120),#27699);
#110=STYLED_ITEM('',(#27804),#120);
#120=MANIFOLD_SOLID_BREP('Body1',#3836);
#136=FACE_BOUND('',#701,.T.);
#137=FACE_BOUND('',#703,.T.);
#175=PLANE('',#4000);
#176=PLANE('',#4001);
#177=PLANE('',#4002);
#178=PLANE('',#4003);
#179=PLANE('',#4004);
#180=PLANE('',#4005);
#181=PLANE('',#4006);
#182=PLANE('',#4007);
#232=CIRCLE('',#3995,4.433);
#233=CIRCLE('',#3996,4.433);
#234=CIRCLE('',#3998,3.72275);
#235=CIRCLE('',#3999,3.72275);
#351=CYLINDRICAL_SURFACE('',#3994,4.433);
#352=CYLINDRICAL_SURFACE('',#3997,3.72275);
#461=FACE_OUTER_BOUND('',#690,.T.);
#462=FACE_OUTER_BOUND('',#691,.T.);
#463=FACE_OUTER_BOUND('',#692,.T.);
#464=FACE_OUTER_BOUND('',#693,.T.);
#465=FACE_OUTER_BOUND('',#694,.T.);
#466=FACE_OUTER_BOUND('',#695,.T.);
#467=FACE_OUTER_BOUND('',#696,.T.);
#468=FACE_OUTER_BOUND('',#697,.T.);
#469=FACE_OUTER_BOUND('',#698,.T.);
#470=FACE_OUTER_BOUND('',#699,.T.);
#471=FACE_OUTER_BOUND('',#700,.T.);
#472=FACE_OUTER_BOUND('',#702,.T.);
#690=EDGE_LOOP('',(#2559,#2560,#2561,#2562));
#691=EDGE_LOOP('',(#2563,#2564,#2565,#2566));
#692=EDGE_LOOP('',(#2567,#2568,#2569,#2570));
#693=EDGE_LOOP('',(#2571,#2572,#2573,#2574));
#694=EDGE_LOOP('',(#2575,#2576,#2577,#2578));
#695=EDGE_LOOP('',(#2579,#2580,#2581,#2582));
#696=EDGE_LOOP('',(#2583,#2584,#2585,#2586));
#697=EDGE_LOOP('',(#2587,#2588,#2589,#2590));
#698=EDGE_LOOP('',(#2591,#2592,#2593,#2594));
#699=EDGE_LOOP('',(#2595,#2596,#2597,#2598));
#700=EDGE_LOOP('',(#2599,#2600,#2601,#2602,#2603,#2604));
#701=EDGE_LOOP('',(#2605,#2606,#2607,#2608));
#702=EDGE_LOOP('',(#2609,#2610,#2611,#2612,#2613,#2614));
#703=EDGE_LOOP('',(#2615,#2616,#2617,#2618));
#944=LINE('',#5461,#1120);
#945=LINE('',#5477,#1121);
#946=LINE('',#5483,#1122);
#947=LINE('',#5542,#1123);
#948=LINE('',#5549,#1124);
#949=LINE('',#5551,#1125);
#950=LINE('',#5553,#1126);
#951=LINE('',#5554,#1127);
#952=LINE('',#5557,#1128);
#953=LINE('',#5559,#1129);
#954=LINE('',#5560,#1130);
#955=LINE('',#5563,#1131);
#956=LINE('',#5565,#1132);
#957=LINE('',#5566,#1133);
#958=LINE('',#5569,#1134);
#959=LINE('',#5571,#1135);
#960=LINE('',#5572,#1136);
#961=LINE('',#5575,#1137);
#962=LINE('',#5577,#1138);
#963=LINE('',#5578,#1139);
#964=LINE('',#5580,#1140);
#965=LINE('',#5581,#1141);
#1120=VECTOR('',#4395,10.);
#1121=VECTOR('',#4396,10.);
#1122=VECTOR('',#4403,10.);
#1123=VECTOR('',#4404,10.);
#1124=VECTOR('',#4413,10.);
#1125=VECTOR('',#4414,10.);
#1126=VECTOR('',#4415,10.);
#1127=VECTOR('',#4416,10.);
#1128=VECTOR('',#4419,9.99999999999998);
#1129=VECTOR('',#4420,9.99999999999998);
#1130=VECTOR('',#4421,10.);
#1131=VECTOR('',#4424,10.);
#1132=VECTOR('',#4425,10.);
#1133=VECTOR('',#4426,10.);
#1134=VECTOR('',#4429,10.);
#1135=VECTOR('',#4430,10.);
#1136=VECTOR('',#4431,10.);
#1137=VECTOR('',#4434,10.);
#1138=VECTOR('',#4435,10.);
#1139=VECTOR('',#4436,10.);
#1140=VECTOR('',#4439,10.);
#1141=VECTOR('',#4440,10.);
#1275=B_SPLINE_CURVE_WITH_KNOTS('',3,(#5446,#5447,#5448,#5449,#5450,#5451,
#5452,#5453,#5454,#5455,#5456,#5457,#5458,#5459),.UNSPECIFIED.,.F.,.F.,
(4,2,2,2,2,2,4),(-0.844212290556731,-0.730966332817565,-0.619975754240938,
-0.457326579004558,-0.29977928179387,-0.147336283383114,0.),
 .UNSPECIFIED.);
#1276=B_SPLINE_CURVE_WITH_KNOTS('',3,(#5463,#5464,#5465,#5466,#5467,#5468,
#5469,#5470,#5471,#5472,#5473,#5474,#5475,#5476),.UNSPECIFIED.,.F.,.F.,
(4,2,2,2,2,2,4),(-0.844212290556731,-0.730966332817565,-0.619975754240938,
-0.457326579004558,-0.29977928179387,-0.147336283383114,0.),
 .UNSPECIFIED.);
#1277=B_SPLINE_CURVE_WITH_KNOTS('',3,(#5513,#5514,#5515,#5516,#5517,#5518,
#5519,#5520,#5521,#5522,#5523,#5524,#5525,#5526),.UNSPECIFIED.,.F.,.F.,
(4,2,2,2,2,2,4),(-0.847325527525843,-0.749719327139836,-0.649860858750851,
-0.495073659399383,-0.335166304629316,-0.170141007879843,0.),
 .UNSPECIFIED.);
#1278=B_SPLINE_CURVE_WITH_KNOTS('',3,(#5528,#5529,#5530,#5531,#5532,#5533,
#5534,#5535,#5536,#5537,#5538,#5539,#5540,#5541),.UNSPECIFIED.,.F.,.F.,
(4,2,2,2,2,2,4),(-0.847325527525843,-0.749719327139836,-0.649860858750851,
-0.495073659399383,-0.335166304629316,-0.170141007879843,0.),
 .UNSPECIFIED.);
#1555=VERTEX_POINT('',#5444);
#1556=VERTEX_POINT('',#5445);
#1557=VERTEX_POINT('',#5460);
#1558=VERTEX_POINT('',#5462);
#1559=VERTEX_POINT('',#5479);
#1560=VERTEX_POINT('',#5481);
#1561=VERTEX_POINT('',#5512);
#1562=VERTEX_POINT('',#5527);
#1563=VERTEX_POINT('',#5547);
#1564=VERTEX_POINT('',#5548);
#1565=VERTEX_POINT('',#5550);
#1566=VERTEX_POINT('',#5552);
#1567=VERTEX_POINT('',#5556);
#1568=VERTEX_POINT('',#5558);
#1569=VERTEX_POINT('',#5562);
#1570=VERTEX_POINT('',#5564);
#1571=VERTEX_POINT('',#5568);
#1572=VERTEX_POINT('',#5570);
#1573=VERTEX_POINT('',#5574);
#1574=VERTEX_POINT('',#5576);
#1949=EDGE_CURVE('',#1555,#1556,#1275,.T.);
#1950=EDGE_CURVE('',#1556,#1557,#944,.T.);
#1951=EDGE_CURVE('',#1558,#1557,#1276,.T.);
#1952=EDGE_CURVE('',#1555,#1558,#945,.T.);
#1953=EDGE_CURVE('',#1559,#1555,#232,.T.);
#1954=EDGE_CURVE('',#1560,#1558,#233,.T.);
#1955=EDGE_CURVE('',#1559,#1560,#946,.T.);
#1956=EDGE_CURVE('',#1561,#1559,#1277,.T.);
#1957=EDGE_CURVE('',#1562,#1560,#1278,.T.);
#1958=EDGE_CURVE('',#1561,#1562,#947,.T.);
#1959=EDGE_CURVE('',#1556,#1561,#234,.T.);
#1960=EDGE_CURVE('',#1557,#1562,#235,.T.);
#1961=EDGE_CURVE('',#1563,#1564,#948,.T.);
#1962=EDGE_CURVE('',#1564,#1565,#949,.T.);
#1963=EDGE_CURVE('',#1566,#1565,#950,.T.);
#1964=EDGE_CURVE('',#1563,#1566,#951,.T.);
#1965=EDGE_CURVE('',#1567,#1563,#952,.T.);
#1966=EDGE_CURVE('',#1568,#1566,#953,.T.);
#1967=EDGE_CURVE('',#1567,#1568,#954,.T.);
#1968=EDGE_CURVE('',#1569,#1567,#955,.T.);
#1969=EDGE_CURVE('',#1570,#1568,#956,.T.);
#1970=EDGE_CURVE('',#1569,#1570,#957,.T.);
#1971=EDGE_CURVE('',#1571,#1569,#958,.T.);
#1972=EDGE_CURVE('',#1572,#1570,#959,.T.);
#1973=EDGE_CURVE('',#1571,#1572,#960,.T.);
#1974=EDGE_CURVE('',#1573,#1571,#961,.T.);
#1975=EDGE_CURVE('',#1574,#1572,#962,.T.);
#1976=EDGE_CURVE('',#1573,#1574,#963,.T.);
#1977=EDGE_CURVE('',#1564,#1573,#964,.T.);
#1978=EDGE_CURVE('',#1565,#1574,#965,.T.);
#2559=ORIENTED_EDGE('',*,*,#1949,.T.);
#2560=ORIENTED_EDGE('',*,*,#1950,.T.);
#2561=ORIENTED_EDGE('',*,*,#1951,.F.);
#2562=ORIENTED_EDGE('',*,*,#1952,.F.);
#2563=ORIENTED_EDGE('',*,*,#1953,.T.);
#2564=ORIENTED_EDGE('',*,*,#1952,.T.);
#2565=ORIENTED_EDGE('',*,*,#1954,.F.);
#2566=ORIENTED_EDGE('',*,*,#1955,.F.);
#2567=ORIENTED_EDGE('',*,*,#1956,.T.);
#2568=ORIENTED_EDGE('',*,*,#1955,.T.);
#2569=ORIENTED_EDGE('',*,*,#1957,.F.);
#2570=ORIENTED_EDGE('',*,*,#1958,.F.);
#2571=ORIENTED_EDGE('',*,*,#1959,.T.);
#2572=ORIENTED_EDGE('',*,*,#1958,.T.);
#2573=ORIENTED_EDGE('',*,*,#1960,.F.);
#2574=ORIENTED_EDGE('',*,*,#1950,.F.);
#2575=ORIENTED_EDGE('',*,*,#1961,.T.);
#2576=ORIENTED_EDGE('',*,*,#1962,.T.);
#2577=ORIENTED_EDGE('',*,*,#1963,.F.);
#2578=ORIENTED_EDGE('',*,*,#1964,.F.);
#2579=ORIENTED_EDGE('',*,*,#1965,.T.);
#2580=ORIENTED_EDGE('',*,*,#1964,.T.);
#2581=ORIENTED_EDGE('',*,*,#1966,.F.);
#2582=ORIENTED_EDGE('',*,*,#1967,.F.);
#2583=ORIENTED_EDGE('',*,*,#1968,.T.);
#2584=ORIENTED_EDGE('',*,*,#1967,.T.);
#2585=ORIENTED_EDGE('',*,*,#1969,.F.);
#2586=ORIENTED_EDGE('',*,*,#1970,.F.);
#2587=ORIENTED_EDGE('',*,*,#1971,.T.);
#2588=ORIENTED_EDGE('',*,*,#1970,.T.);
#2589=ORIENTED_EDGE('',*,*,#1972,.F.);
#2590=ORIENTED_EDGE('',*,*,#1973,.F.);
#2591=ORIENTED_EDGE('',*,*,#1974,.T.);
#2592=ORIENTED_EDGE('',*,*,#1973,.T.);
#2593=ORIENTED_EDGE('',*,*,#1975,.F.);
#2594=ORIENTED_EDGE('',*,*,#1976,.F.);
#2595=ORIENTED_EDGE('',*,*,#1977,.T.);
#2596=ORIENTED_EDGE('',*,*,#1976,.T.);
#2597=ORIENTED_EDGE('',*,*,#1978,.F.);
#2598=ORIENTED_EDGE('',*,*,#1962,.F.);
#2599=ORIENTED_EDGE('',*,*,#1978,.T.);
#2600=ORIENTED_EDGE('',*,*,#1975,.T.);
#2601=ORIENTED_EDGE('',*,*,#1972,.T.);
#2602=ORIENTED_EDGE('',*,*,#1969,.T.);
#2603=ORIENTED_EDGE('',*,*,#1966,.T.);
#2604=ORIENTED_EDGE('',*,*,#1963,.T.);
#2605=ORIENTED_EDGE('',*,*,#1960,.T.);
#2606=ORIENTED_EDGE('',*,*,#1957,.T.);
#2607=ORIENTED_EDGE('',*,*,#1954,.T.);
#2608=ORIENTED_EDGE('',*,*,#1951,.T.);
#2609=ORIENTED_EDGE('',*,*,#1977,.F.);
#2610=ORIENTED_EDGE('',*,*,#1961,.F.);
#2611=ORIENTED_EDGE('',*,*,#1965,.F.);
#2612=ORIENTED_EDGE('',*,*,#1968,.F.);
#2613=ORIENTED_EDGE('',*,*,#1971,.F.);
#2614=ORIENTED_EDGE('',*,*,#1974,.F.);
#2615=ORIENTED_EDGE('',*,*,#1959,.F.);
#2616=ORIENTED_EDGE('',*,*,#1949,.F.);
#2617=ORIENTED_EDGE('',*,*,#1953,.F.);
#2618=ORIENTED_EDGE('',*,*,#1956,.F.);
#3577=B_SPLINE_SURFACE_WITH_KNOTS('',3,1,((#5416,#5417),(#5418,#5419),(#5420,
#5421),(#5422,#5423),(#5424,#5425),(#5426,#5427),(#5428,#5429),(#5430,#5431),
(#5432,#5433),(#5434,#5435),(#5436,#5437),(#5438,#5439),(#5440,#5441),(#5442,
#5443)),.UNSPECIFIED.,.F.,.F.,.F.,(4,2,2,2,2,2,4),(2,2),(-0.844212290556731,
-0.730966332817565,-0.619975754240938,-0.457326579004558,-0.29977928179387,
-0.147336283383114,0.),(0.,0.576),.UNSPECIFIED.);
#3578=B_SPLINE_SURFACE_WITH_KNOTS('',3,1,((#5484,#5485),(#5486,#5487),(#5488,
#5489),(#5490,#5491),(#5492,#5493),(#5494,#5495),(#5496,#5497),(#5498,#5499),
(#5500,#5501),(#5502,#5503),(#5504,#5505),(#5506,#5507),(#5508,#5509),(#5510,
#5511)),.UNSPECIFIED.,.F.,.F.,.F.,(4,2,2,2,2,2,4),(2,2),(-0.847325527525843,
-0.749719327139836,-0.649860858750851,-0.495073659399383,-0.335166304629316,
-0.170141007879843,0.),(0.,0.576),.UNSPECIFIED.);
#3636=ADVANCED_FACE('',(#461),#3577,.T.);
#3637=ADVANCED_FACE('',(#462),#351,.F.);
#3638=ADVANCED_FACE('',(#463),#3578,.T.);
#3639=ADVANCED_FACE('',(#464),#352,.F.);
#3640=ADVANCED_FACE('',(#465),#175,.T.);
#3641=ADVANCED_FACE('',(#466),#176,.T.);
#3642=ADVANCED_FACE('',(#467),#177,.T.);
#3643=ADVANCED_FACE('',(#468),#178,.T.);
#3644=ADVANCED_FACE('',(#469),#179,.T.);
#3645=ADVANCED_FACE('',(#470),#180,.T.);
#3646=ADVANCED_FACE('',(#471,#136),#181,.T.);
#3647=ADVANCED_FACE('',(#472,#137),#182,.F.);
#3836=CLOSED_SHELL('',(#3636,#3637,#3638,#3639,#3640,#3641,#3642,#3643,
#3644,#3645,#3646,#3647));
#3993=AXIS2_PLACEMENT_3D('',#5415,#4393,#4394);
#3994=AXIS2_PLACEMENT_3D('',#5478,#4397,#4398);
#3995=AXIS2_PLACEMENT_3D('',#5480,#4399,#4400);
#3996=AXIS2_PLACEMENT_3D('',#5482,#4401,#4402);
#3997=AXIS2_PLACEMENT_3D('',#5543,#4405,#4406);
#3998=AXIS2_PLACEMENT_3D('',#5544,#4407,#4408);
#3999=AXIS2_PLACEMENT_3D('',#5545,#4409,#4410);
#4000=AXIS2_PLACEMENT_3D('',#5546,#4411,#4412);
#4001=AXIS2_PLACEMENT_3D('',#5555,#4417,#4418);
#4002=AXIS2_PLACEMENT_3D('',#5561,#4422,#4423);
#4003=AXIS2_PLACEMENT_3D('',#5567,#4427,#4428);
#4004=AXIS2_PLACEMENT_3D('',#5573,#4432,#4433);
#4005=AXIS2_PLACEMENT_3D('',#5579,#4437,#4438);
#4006=AXIS2_PLACEMENT_3D('',#5582,#4441,#4442);
#4007=AXIS2_PLACEMENT_3D('',#5583,#4443,#4444);
#4393=DIRECTION('axis',(0.,0.,1.));
#4394=DIRECTION('refdir',(1.,0.,0.));
#4395=DIRECTION('',(1.,0.,0.));
#4396=DIRECTION('',(1.,0.,0.));
#4397=DIRECTION('center_axis',(1.,0.,0.));
#4398=DIRECTION('ref_axis',(0.,0.444750988585694,0.895654262621492));
#4399=DIRECTION('center_axis',(-1.,0.,0.));
#4400=DIRECTION('ref_axis',(0.,0.444750988585694,0.895654262621492));
#4401=DIRECTION('center_axis',(-1.,0.,0.));
#4402=DIRECTION('ref_axis',(0.,0.444750988585694,0.895654262621492));
#4403=DIRECTION('',(1.,0.,0.));
#4404=DIRECTION('',(1.,0.,0.));
#4405=DIRECTION('center_axis',(1.,0.,0.));
#4406=DIRECTION('ref_axis',(0.,-0.580623944517215,-0.814171870708679));
#4407=DIRECTION('center_axis',(-1.,0.,0.));
#4408=DIRECTION('ref_axis',(0.,-0.580623944517215,-0.814171870708679));
#4409=DIRECTION('center_axis',(-1.,0.,0.));
#4410=DIRECTION('ref_axis',(0.,-0.580623944517215,-0.814171870708679));
#4411=DIRECTION('center_axis',(0.,0.866025403784439,0.5));
#4412=DIRECTION('ref_axis',(0.,-0.5,0.866025403784439));
#4413=DIRECTION('',(0.,-0.5,0.866025403784439));
#4414=DIRECTION('',(1.,0.,0.));
#4415=DIRECTION('',(0.,-0.5,0.866025403784439));
#4416=DIRECTION('',(1.,0.,0.));
#4417=DIRECTION('center_axis',(0.,0.866025403784438,-0.5));
#4418=DIRECTION('ref_axis',(0.,0.5,0.866025403784438));
#4419=DIRECTION('',(0.,0.5,0.866025403784438));
#4420=DIRECTION('',(0.,0.5,0.866025403784438));
#4421=DIRECTION('',(1.,0.,0.));
#4422=DIRECTION('center_axis',(0.,-3.02823770847138E-16,-1.));
#4423=DIRECTION('ref_axis',(0.,1.,-3.02823770847138E-16));
#4424=DIRECTION('',(0.,1.,-3.02823770847138E-16));
#4425=DIRECTION('',(0.,1.,-3.02823770847138E-16));
#4426=DIRECTION('',(1.,0.,0.));
#4427=DIRECTION('center_axis',(0.,-0.866025403784439,-0.5));
#4428=DIRECTION('ref_axis',(0.,0.5,-0.866025403784439));
#4429=DIRECTION('',(0.,0.5,-0.866025403784439));
#4430=DIRECTION('',(0.,0.5,-0.866025403784439));
#4431=DIRECTION('',(1.,0.,0.));
#4432=DIRECTION('center_axis',(0.,-0.866025403784439,0.5));
#4433=DIRECTION('ref_axis',(0.,-0.5,-0.866025403784439));
#4434=DIRECTION('',(0.,-0.5,-0.866025403784439));
#4435=DIRECTION('',(0.,-0.5,-0.866025403784439));
#4436=DIRECTION('',(1.,0.,0.));
#4437=DIRECTION('center_axis',(0.,6.05647541694275E-16,1.));
#4438=DIRECTION('ref_axis',(0.,-1.,6.05647541694275E-16));
#4439=DIRECTION('',(0.,-1.,6.05647541694275E-16));
#4440=DIRECTION('',(0.,-1.,6.05647541694275E-16));
#4441=DIRECTION('center_axis',(1.,0.,0.));
#4442=DIRECTION('ref_axis',(0.,1.,0.));
#4443=DIRECTION('center_axis',(1.,0.,0.));
#4444=DIRECTION('ref_axis',(0.,1.,0.));
#5415=CARTESIAN_POINT('',(0.,0.,0.));
#5416=CARTESIAN_POINT('Ctrl Pts',(6.4430005297901,1.97158113240038,3.97043534620107));
#5417=CARTESIAN_POINT('Ctrl Pts',(12.2030005297901,1.97158113240038,3.97043534620107));
#5418=CARTESIAN_POINT('Ctrl Pts',(6.4430005297901,2.29671111436096,3.77621792657107));
#5419=CARTESIAN_POINT('Ctrl Pts',(12.2030005297901,2.29671111436096,3.77621792657107));
#5420=CARTESIAN_POINT('Ctrl Pts',(6.4430005297901,2.59552275281558,3.54102114079632));
#5421=CARTESIAN_POINT('Ctrl Pts',(12.2030005297901,2.59552275281558,3.54102114079632));
#5422=CARTESIAN_POINT('Ctrl Pts',(6.4430005297901,3.11908576775695,3.00435277140383));
#5423=CARTESIAN_POINT('Ctrl Pts',(12.2030005297901,3.11908576775695,3.00435277140383));
#5424=CARTESIAN_POINT('Ctrl Pts',(6.4430005297901,3.34301024132503,2.70651491388494));
#5425=CARTESIAN_POINT('Ctrl Pts',(12.2030005297901,3.34301024132503,2.70651491388494));
#5426=CARTESIAN_POINT('Ctrl Pts',(6.4430005297901,3.79251211736076,1.90981794028965));
#5427=CARTESIAN_POINT('Ctrl Pts',(12.2030005297901,3.79251211736076,1.90981794028965));
#5428=CARTESIAN_POINT('Ctrl Pts',(6.4430005297901,3.96610878107774,1.3893796287376));
#5429=CARTESIAN_POINT('Ctrl Pts',(12.2030005297901,3.96610878107774,1.3893796287376));
#5430=CARTESIAN_POINT('Ctrl Pts',(6.4430005297901,4.09877879619631,0.327978495265378));
#5431=CARTESIAN_POINT('Ctrl Pts',(12.2030005297901,4.09877879619631,0.327978495265378));
#5432=CARTESIAN_POINT('Ctrl Pts',(6.4430005297901,4.06307606785725,-0.201870082003989));
#5433=CARTESIAN_POINT('Ctrl Pts',(12.2030005297901,4.06307606785725,-0.201870082003989));
#5434=CARTESIAN_POINT('Ctrl Pts',(6.4430005297901,3.79206680758235,-1.20058842967181));
#5435=CARTESIAN_POINT('Ctrl Pts',(12.2030005297901,3.79206680758235,-1.20058842967181));
#5436=CARTESIAN_POINT('Ctrl Pts',(6.4430005297901,3.56572122172907,-1.66148594501202));
#5437=CARTESIAN_POINT('Ctrl Pts',(12.2030005297901,3.56572122172907,-1.66148594501202));
#5438=CARTESIAN_POINT('Ctrl Pts',(6.4430005297901,2.95711124459234,-2.45497912282895));
#5439=CARTESIAN_POINT('Ctrl Pts',(12.2030005297901,2.95711124459234,-2.45497912282895));
#5440=CARTESIAN_POINT('Ctrl Pts',(6.4430005297901,2.58595465431403,-2.78386901588454));
#5441=CARTESIAN_POINT('Ctrl Pts',(12.2030005297901,2.58595465431403,-2.78386901588454));
#5442=CARTESIAN_POINT('Ctrl Pts',(6.4430005297901,2.16151778945146,-3.03095833168072));
#5443=CARTESIAN_POINT('Ctrl Pts',(12.2030005297901,2.16151778945146,-3.03095833168072));
#5444=CARTESIAN_POINT('',(6.4430005297901,1.97158113240038,3.97043534620107));
#5445=CARTESIAN_POINT('',(6.4430005297901,2.16151778945147,-3.03095833168073));
#5446=CARTESIAN_POINT('Ctrl Pts',(6.4430005297901,1.97158113240038,3.97043534620107));
#5447=CARTESIAN_POINT('Ctrl Pts',(6.4430005297901,2.29671111436096,3.77621792657107));
#5448=CARTESIAN_POINT('Ctrl Pts',(6.4430005297901,2.59552275281558,3.54102114079632));
#5449=CARTESIAN_POINT('Ctrl Pts',(6.4430005297901,3.11908576775695,3.00435277140383));
#5450=CARTESIAN_POINT('Ctrl Pts',(6.4430005297901,3.34301024132503,2.70651491388494));
#5451=CARTESIAN_POINT('Ctrl Pts',(6.4430005297901,3.79251211736076,1.90981794028965));
#5452=CARTESIAN_POINT('Ctrl Pts',(6.4430005297901,3.96610878107774,1.3893796287376));
#5453=CARTESIAN_POINT('Ctrl Pts',(6.4430005297901,4.09877879619631,0.327978495265378));
#5454=CARTESIAN_POINT('Ctrl Pts',(6.4430005297901,4.06307606785725,-0.201870082003989));
#5455=CARTESIAN_POINT('Ctrl Pts',(6.4430005297901,3.79206680758235,-1.20058842967181));
#5456=CARTESIAN_POINT('Ctrl Pts',(6.4430005297901,3.56572122172907,-1.66148594501202));
#5457=CARTESIAN_POINT('Ctrl Pts',(6.4430005297901,2.95711124459234,-2.45497912282895));
#5458=CARTESIAN_POINT('Ctrl Pts',(6.4430005297901,2.58595465431403,-2.78386901588454));
#5459=CARTESIAN_POINT('Ctrl Pts',(6.4430005297901,2.16151778945146,-3.03095833168072));
#5460=CARTESIAN_POINT('',(10.4430005297901,2.16151778945147,-3.03095833168073));
#5461=CARTESIAN_POINT('',(6.4430005297901,2.16151778945147,-3.03095833168073));
#5462=CARTESIAN_POINT('',(10.4430005297901,1.97158113240038,3.97043534620107));
#5463=CARTESIAN_POINT('Ctrl Pts',(10.4430005297901,1.97158113240038,3.97043534620107));
#5464=CARTESIAN_POINT('Ctrl Pts',(10.4430005297901,2.29671111436096,3.77621792657107));
#5465=CARTESIAN_POINT('Ctrl Pts',(10.4430005297901,2.59552275281558,3.54102114079632));
#5466=CARTESIAN_POINT('Ctrl Pts',(10.4430005297901,3.11908576775695,3.00435277140383));
#5467=CARTESIAN_POINT('Ctrl Pts',(10.4430005297901,3.34301024132503,2.70651491388494));
#5468=CARTESIAN_POINT('Ctrl Pts',(10.4430005297901,3.79251211736076,1.90981794028965));
#5469=CARTESIAN_POINT('Ctrl Pts',(10.4430005297901,3.96610878107774,1.3893796287376));
#5470=CARTESIAN_POINT('Ctrl Pts',(10.4430005297901,4.09877879619631,0.327978495265378));
#5471=CARTESIAN_POINT('Ctrl Pts',(10.4430005297901,4.06307606785725,-0.201870082003989));
#5472=CARTESIAN_POINT('Ctrl Pts',(10.4430005297901,3.79206680758235,-1.20058842967181));
#5473=CARTESIAN_POINT('Ctrl Pts',(10.4430005297901,3.56572122172907,-1.66148594501202));
#5474=CARTESIAN_POINT('Ctrl Pts',(10.4430005297901,2.95711124459234,-2.45497912282895));
#5475=CARTESIAN_POINT('Ctrl Pts',(10.4430005297901,2.58595465431403,-2.78386901588454));
#5476=CARTESIAN_POINT('Ctrl Pts',(10.4430005297901,2.16151778945146,-3.03095833168072));
#5477=CARTESIAN_POINT('',(6.4430005297901,1.97158113240038,3.97043534620107));
#5478=CARTESIAN_POINT('Origin',(6.4430005297901,-2.77555756156289E-16,5.55111512312578E-16));
#5479=CARTESIAN_POINT('',(6.4430005297901,-1.97158113240039,3.97043534620107));
#5480=CARTESIAN_POINT('Origin',(6.4430005297901,-2.77555756156289E-16,5.55111512312578E-16));
#5481=CARTESIAN_POINT('',(10.4430005297901,-1.97158113240039,3.97043534620107));
#5482=CARTESIAN_POINT('Origin',(10.4430005297901,-2.77555756156289E-16,
5.55111512312578E-16));
#5483=CARTESIAN_POINT('',(6.4430005297901,-1.97158113240039,3.97043534620107));
#5484=CARTESIAN_POINT('Ctrl Pts',(6.4430005297901,-2.16151778945139,-3.03095833168078));
#5485=CARTESIAN_POINT('Ctrl Pts',(12.2030005297901,-2.16151778945139,-3.03095833168078));
#5486=CARTESIAN_POINT('Ctrl Pts',(6.4430005297901,-2.4417969811413,-2.86779155838698));
#5487=CARTESIAN_POINT('Ctrl Pts',(12.2030005297901,-2.4417969811413,-2.86779155838698));
#5488=CARTESIAN_POINT('Ctrl Pts',(6.4430005297901,-2.69946597133354,-2.66855779259647));
#5489=CARTESIAN_POINT('Ctrl Pts',(12.2030005297901,-2.69946597133354,-2.66855779259647));
#5490=CARTESIAN_POINT('Ctrl Pts',(6.4430005297901,-3.16313807023027,-2.20413689736136));
#5491=CARTESIAN_POINT('Ctrl Pts',(12.2030005297901,-3.16313807023027,-2.20413689736136));
#5492=CARTESIAN_POINT('Ctrl Pts',(6.4430005297901,-3.36582061002206,-1.93954623621156));
#5493=CARTESIAN_POINT('Ctrl Pts',(12.2030005297901,-3.36582061002206,-1.93954623621156));
#5494=CARTESIAN_POINT('Ctrl Pts',(6.4430005297901,-3.7905877946382,-1.20735040930033));
#5495=CARTESIAN_POINT('Ctrl Pts',(12.2030005297901,-3.7905877946382,-1.20735040930033));
#5496=CARTESIAN_POINT('Ctrl Pts',(6.4430005297901,-3.95787261855977,-0.715467908482556));
#5497=CARTESIAN_POINT('Ctrl Pts',(12.2030005297901,-3.95787261855977,-0.715467908482556));
#5498=CARTESIAN_POINT('Ctrl Pts',(6.4430005297901,-4.0999785741866,0.321696095215354));
#5499=CARTESIAN_POINT('Ctrl Pts',(12.2030005297901,-4.0999785741866,0.321696095215354));
#5500=CARTESIAN_POINT('Ctrl Pts',(6.4430005297901,-4.06691955087291,0.857794436836504));
#5501=CARTESIAN_POINT('Ctrl Pts',(12.2030005297901,-4.06691955087291,0.857794436836504));
#5502=CARTESIAN_POINT('Ctrl Pts',(6.4430005297901,-3.79581350913489,1.90493582172488));
#5503=CARTESIAN_POINT('Ctrl Pts',(12.2030005297901,-3.79581350913489,1.90493582172488));
#5504=CARTESIAN_POINT('Ctrl Pts',(6.4430005297901,-3.55404702294629,2.40416273654669));
#5505=CARTESIAN_POINT('Ctrl Pts',(12.2030005297901,-3.55404702294629,2.40416273654669));
#5506=CARTESIAN_POINT('Ctrl Pts',(6.4430005297901,-2.88474862400959,3.29779955123577));
#5507=CARTESIAN_POINT('Ctrl Pts',(12.2030005297901,-2.88474862400959,3.29779955123577));
#5508=CARTESIAN_POINT('Ctrl Pts',(6.4430005297901,-2.45846445810197,3.67959405679302));
#5509=CARTESIAN_POINT('Ctrl Pts',(12.2030005297901,-2.45846445810197,3.67959405679302));
#5510=CARTESIAN_POINT('Ctrl Pts',(6.4430005297901,-1.9715811324004,3.97043534620107));
#5511=CARTESIAN_POINT('Ctrl Pts',(12.2030005297901,-1.9715811324004,3.97043534620107));
#5512=CARTESIAN_POINT('',(6.4430005297901,-2.16151778945139,-3.03095833168078));
#5513=CARTESIAN_POINT('Ctrl Pts',(6.4430005297901,-2.16151778945139,-3.03095833168078));
#5514=CARTESIAN_POINT('Ctrl Pts',(6.4430005297901,-2.4417969811413,-2.86779155838698));
#5515=CARTESIAN_POINT('Ctrl Pts',(6.4430005297901,-2.69946597133354,-2.66855779259647));
#5516=CARTESIAN_POINT('Ctrl Pts',(6.4430005297901,-3.16313807023027,-2.20413689736136));
#5517=CARTESIAN_POINT('Ctrl Pts',(6.4430005297901,-3.36582061002206,-1.93954623621156));
#5518=CARTESIAN_POINT('Ctrl Pts',(6.4430005297901,-3.7905877946382,-1.20735040930033));
#5519=CARTESIAN_POINT('Ctrl Pts',(6.4430005297901,-3.95787261855977,-0.715467908482556));
#5520=CARTESIAN_POINT('Ctrl Pts',(6.4430005297901,-4.0999785741866,0.321696095215354));
#5521=CARTESIAN_POINT('Ctrl Pts',(6.4430005297901,-4.06691955087291,0.857794436836504));
#5522=CARTESIAN_POINT('Ctrl Pts',(6.4430005297901,-3.79581350913489,1.90493582172488));
#5523=CARTESIAN_POINT('Ctrl Pts',(6.4430005297901,-3.55404702294629,2.40416273654669));
#5524=CARTESIAN_POINT('Ctrl Pts',(6.4430005297901,-2.88474862400959,3.29779955123577));
#5525=CARTESIAN_POINT('Ctrl Pts',(6.4430005297901,-2.45846445810197,3.67959405679302));
#5526=CARTESIAN_POINT('Ctrl Pts',(6.4430005297901,-1.9715811324004,3.97043534620107));
#5527=CARTESIAN_POINT('',(10.4430005297901,-2.16151778945139,-3.03095833168078));
#5528=CARTESIAN_POINT('Ctrl Pts',(10.4430005297901,-2.16151778945139,-3.03095833168078));
#5529=CARTESIAN_POINT('Ctrl Pts',(10.4430005297901,-2.4417969811413,-2.86779155838698));
#5530=CARTESIAN_POINT('Ctrl Pts',(10.4430005297901,-2.69946597133354,-2.66855779259647));
#5531=CARTESIAN_POINT('Ctrl Pts',(10.4430005297901,-3.16313807023027,-2.20413689736136));
#5532=CARTESIAN_POINT('Ctrl Pts',(10.4430005297901,-3.36582061002206,-1.93954623621156));
#5533=CARTESIAN_POINT('Ctrl Pts',(10.4430005297901,-3.7905877946382,-1.20735040930033));
#5534=CARTESIAN_POINT('Ctrl Pts',(10.4430005297901,-3.95787261855977,-0.715467908482556));
#5535=CARTESIAN_POINT('Ctrl Pts',(10.4430005297901,-4.0999785741866,0.321696095215354));
#5536=CARTESIAN_POINT('Ctrl Pts',(10.4430005297901,-4.06691955087291,0.857794436836504));
#5537=CARTESIAN_POINT('Ctrl Pts',(10.4430005297901,-3.79581350913489,1.90493582172488));
#5538=CARTESIAN_POINT('Ctrl Pts',(10.4430005297901,-3.55404702294629,2.40416273654669));
#5539=CARTESIAN_POINT('Ctrl Pts',(10.4430005297901,-2.88474862400959,3.29779955123577));
#5540=CARTESIAN_POINT('Ctrl Pts',(10.4430005297901,-2.45846445810197,3.67959405679302));
#5541=CARTESIAN_POINT('Ctrl Pts',(10.4430005297901,-1.9715811324004,3.97043534620107));
#5542=CARTESIAN_POINT('',(6.4430005297901,-2.16151778945139,-3.03095833168078));
#5543=CARTESIAN_POINT('Origin',(6.4430005297901,-2.77555756156289E-16,5.55111512312578E-16));
#5544=CARTESIAN_POINT('Origin',(6.4430005297901,-2.77555756156289E-16,5.55111512312578E-16));
#5545=CARTESIAN_POINT('Origin',(10.4430005297901,-2.77555756156289E-16,
5.55111512312578E-16));
#5546=CARTESIAN_POINT('Origin',(6.4430005297901,7.33246945257534,-3.33066907387547E-15));
#5547=CARTESIAN_POINT('',(6.4430005297901,7.33246945257534,-3.33066907387547E-15));
#5548=CARTESIAN_POINT('',(6.4430005297901,3.66623472628768,6.35010481840362));
#5549=CARTESIAN_POINT('',(6.4430005297901,7.33246945257534,-3.33066907387547E-15));
#5550=CARTESIAN_POINT('',(10.4430005297901,3.66623472628768,6.35010481840362));
#5551=CARTESIAN_POINT('',(6.4430005297901,3.66623472628768,6.35010481840362));
#5552=CARTESIAN_POINT('',(10.4430005297901,7.33246945257534,-3.33066907387547E-15));
#5553=CARTESIAN_POINT('',(10.4430005297901,7.33246945257534,-3.33066907387547E-15));
#5554=CARTESIAN_POINT('',(6.4430005297901,7.33246945257534,-3.33066907387547E-15));
#5555=CARTESIAN_POINT('Origin',(6.4430005297901,3.66623472628767,-6.35010481840363));
#5556=CARTESIAN_POINT('',(6.4430005297901,3.66623472628767,-6.35010481840363));
#5557=CARTESIAN_POINT('',(6.4430005297901,3.66623472628767,-6.35010481840363));
#5558=CARTESIAN_POINT('',(10.4430005297901,3.66623472628767,-6.35010481840363));
#5559=CARTESIAN_POINT('',(10.4430005297901,3.66623472628767,-6.35010481840363));
#5560=CARTESIAN_POINT('',(6.4430005297901,3.66623472628767,-6.35010481840363));
#5561=CARTESIAN_POINT('Origin',(6.4430005297901,-3.66623472628767,-6.35010481840362));
#5562=CARTESIAN_POINT('',(6.4430005297901,-3.66623472628767,-6.35010481840362));
#5563=CARTESIAN_POINT('',(6.4430005297901,-3.66623472628767,-6.35010481840362));
#5564=CARTESIAN_POINT('',(10.4430005297901,-3.66623472628767,-6.35010481840362));
#5565=CARTESIAN_POINT('',(10.4430005297901,-3.66623472628767,-6.35010481840362));
#5566=CARTESIAN_POINT('',(6.4430005297901,-3.66623472628767,-6.35010481840362));
#5567=CARTESIAN_POINT('Origin',(6.4430005297901,-7.33246945257535,2.77555756156289E-15));
#5568=CARTESIAN_POINT('',(6.4430005297901,-7.33246945257535,2.77555756156289E-15));
#5569=CARTESIAN_POINT('',(6.4430005297901,-7.33246945257535,2.77555756156289E-15));
#5570=CARTESIAN_POINT('',(10.4430005297901,-7.33246945257535,2.77555756156289E-15));
#5571=CARTESIAN_POINT('',(10.4430005297901,-7.33246945257535,2.77555756156289E-15));
#5572=CARTESIAN_POINT('',(6.4430005297901,-7.33246945257535,2.77555756156289E-15));
#5573=CARTESIAN_POINT('Origin',(6.4430005297901,-3.66623472628767,6.35010481840363));
#5574=CARTESIAN_POINT('',(6.4430005297901,-3.66623472628767,6.35010481840363));
#5575=CARTESIAN_POINT('',(6.4430005297901,-3.66623472628767,6.35010481840363));
#5576=CARTESIAN_POINT('',(10.4430005297901,-3.66623472628767,6.35010481840363));
#5577=CARTESIAN_POINT('',(10.4430005297901,-3.66623472628767,6.35010481840363));
#5578=CARTESIAN_POINT('',(6.4430005297901,-3.66623472628767,6.35010481840363));
#5579=CARTESIAN_POINT('Origin',(6.4430005297901,3.66623472628768,6.35010481840362));
#5580=CARTESIAN_POINT('',(6.4430005297901,3.66623472628768,6.35010481840362));
#5581=CARTESIAN_POINT('',(10.4430005297901,3.66623472628768,6.35010481840362));
#5582=CARTESIAN_POINT('Origin',(10.4430005297901,0.,0.));
#5583=CARTESIAN_POINT('Origin',(6.4430005297901,0.,0.));
#27687=UNCERTAINTY_MEASURE_WITH_UNIT(LENGTH_MEASURE(0.01),#27708,
'DISTANCE_ACCURACY_VALUE',
'Maximum model space distance between geometric entities at asserted c
onnectivities');
#27695=UNCERTAINTY_MEASURE_WITH_UNIT(LENGTH_MEASURE(0.01),#27708,
'DISTANCE_ACCURACY_VALUE',
'Maximum model space distance between geometric entities at asserted c
onnectivities');
#27699=(
GEOMETRIC_REPRESENTATION_CONTEXT(3)
GLOBAL_UNCERTAINTY_ASSIGNED_CONTEXT((#27687))
GLOBAL_UNIT_ASSIGNED_CONTEXT((#27708,#27710,#27711))
REPRESENTATION_CONTEXT('','3D')
);
#27707=(
GEOMETRIC_REPRESENTATION_CONTEXT(3)
GLOBAL_UNCERTAINTY_ASSIGNED_CONTEXT((#27695))
GLOBAL_UNIT_ASSIGNED_CONTEXT((#27708,#27710,#27711))
REPRESENTATION_CONTEXT('','3D')
);
#27708=(
LENGTH_UNIT()
NAMED_UNIT(*)
SI_UNIT(.MILLI.,.METRE.)
);
#27710=(
NAMED_UNIT(*)
PLANE_ANGLE_UNIT()
SI_UNIT($,.RADIAN.)
);
#27711=(
NAMED_UNIT(*)
SI_UNIT($,.STERADIAN.)
SOLID_ANGLE_UNIT()
);
#27715=SHAPE_DEFINITION_REPRESENTATION(#27726,#27747);
#27726=PRODUCT_DEFINITION_SHAPE('',$,#27759);
#27747=SHAPE_REPRESENTATION('',(#3993),#27699);
#27755=PRODUCT_DEFINITION_CONTEXT('part definition',#27790,'design');
#27759=PRODUCT_DEFINITION('Nut_02','Nut_02',#27770,#27755);
#27770=PRODUCT_DEFINITION_FORMATION('',$,#27795);
#27790=APPLICATION_CONTEXT(
'Core Data for Automotive Mechanical Design Process');
#27791=PRODUCT_CONTEXT('part definition',#27790,'mechanical');
#27795=PRODUCT('Nut_02','Nut_02',$,(#27791));
#27804=PRESENTATION_STYLE_ASSIGNMENT((#27806));
#27806=SURFACE_STYLE_USAGE(.BOTH.,#27808);
#27808=SURFACE_SIDE_STYLE('',(#27810));
#27810=SURFACE_STYLE_FILL_AREA(#27812);
#27812=FILL_AREA_STYLE('Opaque(160,160,160)',(#27814));
#27814=FILL_AREA_STYLE_COLOUR('Opaque(160,160,160)',#27816);
#27816=COLOUR_RGB('Opaque(160,160,160)', 0.09019608, 0.27058824, 0.51372549);
ENDSEC;
END-ISO-10303-21;
